ISO-10303-21;
HEADER;
/* Generated by software containing ST-Developer
 * from STEP Tools, Inc. (www.steptools.com) 
 */

FILE_DESCRIPTION(
/* description */ ('Bin tilter linkage'),
/* implementation_level */ '2;1');

FILE_NAME(
/* name */ 'Screw keeper fastener.step',
/* time_stamp */ '2026-10-28T03:26:24-07:00',
/* author */ (''),
/* organization */ (''),
/* preprocessor_version */ 'ST-DEVELOPER v20.2',
/* originating_system */ 'Autodesk Translation Framework v15.17.0.0',
/* authorisation */ '');

FILE_SCHEMA (('AUTOMOTIVE_DESIGN { 1 0 10303 214 3 1 1 }'));
ENDSEC;

DATA;
#10=MECHANICAL_DESIGN_GEOMETRIC_PRESENTATION_REPRESENTATION('',(#877),#23728);
#665=SHAPE_REPRESENTATION_RELATIONSHIP('SRR','None',#24129,#771);
#771=ADVANCED_BREP_SHAPE_REPRESENTATION('',(#991),#23629);
#877=STYLED_ITEM('',(#24772),#991);
#991=MANIFOLD_SOLID_BREP('Body1',#12407);
#1193=FACE_BOUND('',#2915,.T.);
#1563=PLANE('',#13975);
#1564=PLANE('',#13980);
#1565=PLANE('',#13983);
#2031=FACE_OUTER_BOUND('',#2914,.T.);
#2032=FACE_OUTER_BOUND('',#2916,.T.);
#2033=FACE_OUTER_BOUND('',#2917,.T.);
#2034=FACE_OUTER_BOUND('',#2918,.T.);
#2035=FACE_OUTER_BOUND('',#2919,.T.);
#2914=EDGE_LOOP('',(#8991));
#2915=EDGE_LOOP('',(#8992));
#2916=EDGE_LOOP('',(#8993,#8994,#8995,#8996));
#2917=EDGE_LOOP('',(#8997));
#2918=EDGE_LOOP('',(#8998,#8999,#9000,#9001));
#2919=EDGE_LOOP('',(#9002));
#4018=LINE('',#20426,#4693);
#4019=LINE('',#20432,#4694);
#4693=VECTOR('',#16249,0.35);
#4694=VECTOR('',#16258,0.199999999999999);
#5339=CIRCLE('',#13976,0.35);
#5340=CIRCLE('',#13977,0.199999999999999);
#5341=CIRCLE('',#13979,0.35);
#5342=CIRCLE('',#13982,0.199999999999999);
#6163=VERTEX_POINT('',#20420);
#6164=VERTEX_POINT('',#20422);
#6165=VERTEX_POINT('',#20425);
#6166=VERTEX_POINT('',#20430);
#7235=EDGE_CURVE('',#6163,#6163,#5339,.T.);
#7236=EDGE_CURVE('',#6164,#6164,#5340,.T.);
#7237=EDGE_CURVE('',#6163,#6165,#4018,.T.);
#7238=EDGE_CURVE('',#6165,#6165,#5341,.T.);
#7239=EDGE_CURVE('',#6166,#6166,#5342,.T.);
#7240=EDGE_CURVE('',#6166,#6164,#4019,.T.);
#8991=ORIENTED_EDGE('',*,*,#7235,.T.);
#8992=ORIENTED_EDGE('',*,*,#7236,.F.);
#8993=ORIENTED_EDGE('',*,*,#7235,.F.);
#8994=ORIENTED_EDGE('',*,*,#7237,.T.);
#8995=ORIENTED_EDGE('',*,*,#7238,.T.);
#8996=ORIENTED_EDGE('',*,*,#7237,.F.);
#8997=ORIENTED_EDGE('',*,*,#7238,.F.);
#8998=ORIENTED_EDGE('',*,*,#7239,.F.);
#8999=ORIENTED_EDGE('',*,*,#7240,.T.);
#9000=ORIENTED_EDGE('',*,*,#7236,.T.);
#9001=ORIENTED_EDGE('',*,*,#7240,.F.);
#9002=ORIENTED_EDGE('',*,*,#7239,.T.);
#11337=CYLINDRICAL_SURFACE('',#13978,0.35);
#11338=CYLINDRICAL_SURFACE('',#13981,0.199999999999999);
#11756=ADVANCED_FACE('',(#2031,#1193),#1563,.T.);
#11757=ADVANCED_FACE('',(#2032),#11337,.T.);
#11758=ADVANCED_FACE('',(#2033),#1564,.F.);
#11759=ADVANCED_FACE('',(#2034),#11338,.T.);
#11760=ADVANCED_FACE('',(#2035),#1565,.T.);
#12407=CLOSED_SHELL('',(#11756,#11757,#11758,#11759,#11760));
#13974=AXIS2_PLACEMENT_3D('',#20418,#16239,#16240);
#13975=AXIS2_PLACEMENT_3D('',#20419,#16241,#16242);
#13976=AXIS2_PLACEMENT_3D('',#20421,#16243,#16244);
#13977=AXIS2_PLACEMENT_3D('',#20423,#16245,#16246);
#13978=AXIS2_PLACEMENT_3D('',#20424,#16247,#16248);
#13979=AXIS2_PLACEMENT_3D('',#20427,#16250,#16251);
#13980=AXIS2_PLACEMENT_3D('',#20428,#16252,#16253);
#13981=AXIS2_PLACEMENT_3D('',#20429,#16254,#16255);
#13982=AXIS2_PLACEMENT_3D('',#20431,#16256,#16257);
#13983=AXIS2_PLACEMENT_3D('',#20433,#16259,#16260);
#16239=DIRECTION('axis',(0.,0.,1.));
#16240=DIRECTION('refdir',(1.,0.,0.));
#16241=DIRECTION('center_axis',(1.,0.,0.));
#16242=DIRECTION('ref_axis',(0.,0.,-1.));
#16243=DIRECTION('center_axis',(1.,0.,0.));
#16244=DIRECTION('ref_axis',(0.,0.,-1.));
#16245=DIRECTION('center_axis',(1.,0.,0.));
#16246=DIRECTION('ref_axis',(0.,0.,-1.));
#16247=DIRECTION('center_axis',(1.,0.,0.));
#16248=DIRECTION('ref_axis',(0.,0.,-1.));
#16249=DIRECTION('',(-1.,0.,0.));
#16250=DIRECTION('center_axis',(1.,0.,0.));
#16251=DIRECTION('ref_axis',(0.,0.,-1.));
#16252=DIRECTION('center_axis',(1.,0.,0.));
#16253=DIRECTION('ref_axis',(0.,0.,-1.));
#16254=DIRECTION('center_axis',(1.,0.,0.));
#16255=DIRECTION('ref_axis',(0.,0.,-1.));
#16256=DIRECTION('center_axis',(1.,0.,0.));
#16257=DIRECTION('ref_axis',(0.,0.,-1.));
#16258=DIRECTION('',(-1.,0.,0.));
#16259=DIRECTION('center_axis',(1.,0.,0.));
#16260=DIRECTION('ref_axis',(0.,0.,-1.));
#20418=CARTESIAN_POINT('',(0.,0.,0.));
#20419=CARTESIAN_POINT('Origin',(-10.2,-4.5,9.85));
#20420=CARTESIAN_POINT('',(-10.2,-4.5,10.2));
#20421=CARTESIAN_POINT('Origin',(-10.2,-4.5,9.85));
#20422=CARTESIAN_POINT('',(-10.2,-4.5,10.05));
#20423=CARTESIAN_POINT('Origin',(-10.2,-4.5,9.85));
#20424=CARTESIAN_POINT('Origin',(-10.6,-4.5,9.85));
#20425=CARTESIAN_POINT('',(-10.6,-4.5,10.2));
#20426=CARTESIAN_POINT('',(-10.6,-4.5,10.2));
#20427=CARTESIAN_POINT('Origin',(-10.6,-4.5,9.85));
#20428=CARTESIAN_POINT('Origin',(-10.6,-4.5,9.85));
#20429=CARTESIAN_POINT('Origin',(-10.2,-4.5,9.85));
#20430=CARTESIAN_POINT('',(-9.5,-4.5,10.05));
#20431=CARTESIAN_POINT('Origin',(-9.5,-4.5,9.85));
#20432=CARTESIAN_POINT('',(-10.2,-4.5,10.05));
#20433=CARTESIAN_POINT('Origin',(-9.5,-4.5,9.85));
#23512=UNCERTAINTY_MEASURE_WITH_UNIT(LENGTH_MEASURE(0.001),#23729,
'DISTANCE_ACCURACY_VALUE',
'Maximum model space distance between geometric entities at asserted c
onnectivities');
#23611=UNCERTAINTY_MEASURE_WITH_UNIT(LENGTH_MEASURE(0.001),#23729,
'DISTANCE_ACCURACY_VALUE',
'Maximum model space distance between geometric entities at asserted c
onnectivities');
#23629=(
GEOMETRIC_REPRESENTATION_CONTEXT(3)
GLOBAL_UNCERTAINTY_ASSIGNED_CONTEXT((#23512))
GLOBAL_UNIT_ASSIGNED_CONTEXT((#23729,#23731,#23732))
REPRESENTATION_CONTEXT('','3D')
);
#23728=(
GEOMETRIC_REPRESENTATION_CONTEXT(3)
GLOBAL_UNCERTAINTY_ASSIGNED_CONTEXT((#23611))
GLOBAL_UNIT_ASSIGNED_CONTEXT((#23729,#23731,#23732))
REPRESENTATION_CONTEXT('','3D')
);
#23729=(
LENGTH_UNIT()
NAMED_UNIT(*)
SI_UNIT(.CENTI.,.METRE.)
);
#23731=(
NAMED_UNIT(*)
PLANE_ANGLE_UNIT()
SI_UNIT($,.RADIAN.)
);
#23732=(
NAMED_UNIT(*)
SI_UNIT($,.STERADIAN.)
SOLID_ANGLE_UNIT()
);
#23750=SHAPE_DEFINITION_REPRESENTATION(#23866,#24129);
#23866=PRODUCT_DEFINITION_SHAPE('',$,#24246);
#24129=SHAPE_REPRESENTATION('',(#13974),#23629);
#24228=PRODUCT_DEFINITION_CONTEXT('part definition',#24578,'design');
#24246=PRODUCT_DEFINITION('Screw keeper fastener',
'Screw keeper fastener',#24362,#24228);
#24362=PRODUCT_DEFINITION_FORMATION('',$,#24597);
#24578=APPLICATION_CONTEXT(
'Core Data for Automotive Mechanical Design Process');
#24579=PRODUCT_CONTEXT('part definition',#24578,'mechanical');
#24597=PRODUCT('Screw keeper fastener','Screw keeper fastener',
'Screw keeper fastener',(#24579));
#24766=COLOUR_RGB('Black',0.12,0.14,0.17);
#24767=FILL_AREA_STYLE_COLOUR('',#24766);
#24768=FILL_AREA_STYLE('',(#24767));
#24769=SURFACE_STYLE_FILL_AREA(#24768);
#24770=SURFACE_SIDE_STYLE('',(#24769));
#24771=SURFACE_STYLE_USAGE(.BOTH.,#24770);
#24772=PRESENTATION_STYLE_ASSIGNMENT((#24771));
ENDSEC;
END-ISO-10303-21;
